ISO-10303-21;
HEADER;
FILE_DESCRIPTION (('STEP AP214'),
    '1' );
FILE_NAME ('rubber for base.step',
    '2026-10-05T20:10:51',
    ( '' ),
    ( '' ),
    'SwSTEP 2.0',
    'SolidWorks 2020',
    '' );
FILE_SCHEMA (( 'AUTOMOTIVE_DESIGN' ));
ENDSEC;

DATA;
#224=SURFACE_STYLE_USAGE ( .BOTH. , #31713 ) ;
#583=CARTESIAN_POINT ( 'NONE',  ( 2.535847408461032609E-15, 11.09999999999999432, -0.2598076211376266764 ) ) ;
#664=DIRECTION ( 'NONE',  ( 1.000000000000000000, 0.000000000000000000, -1.465138070926357285E-17 ) ) ;
#926=UNCERTAINTY_MEASURE_WITH_UNIT (LENGTH_MEASURE( 1.000000000000000082E-05 ), #6639, 'distance_accuracy_value', 'NONE');
#1300=( LENGTH_UNIT ( ) NAMED_UNIT ( * ) SI_UNIT ( .MILLI., .METRE. ) );
#1459=CIRCLE ( 'NONE', #122659, 10.99999999999738698 ) ;
#1814=AXIS2_PLACEMENT_3D ( 'NONE', #77579, #34949, #33893 ) ;
#3366=FACE_OUTER_BOUND ( 'NONE', #203772, .T. ) ;
#4616=SURFACE_SIDE_STYLE ('',( #120620 ) ) ;
#6639=( LENGTH_UNIT ( ) NAMED_UNIT ( * ) SI_UNIT ( .MILLI., .METRE. ) );
#6648=COLOUR_RGB ( '', 0.31764706, 0.68627451, 0.89019608) ;
#6765=( NAMED_UNIT ( * ) SI_UNIT ( $, .STERADIAN. ) SOLID_ANGLE_UNIT ( ) );
#7837=( NAMED_UNIT ( * ) PLANE_ANGLE_UNIT ( ) SI_UNIT ( $, .RADIAN. ) );
#8567=ORIENTED_EDGE ( 'NONE', *, *, #191657, .T. ) ;
#9068=ADVANCED_FACE ( 'NONE', ( #11036 ), #120962, .T. ) ;
#9076=EDGE_LOOP ( 'NONE', ( #141587, #36747, #27725, #90938, #169125, #107784 ) ) ;
#9616=( LENGTH_UNIT ( ) NAMED_UNIT ( * ) SI_UNIT ( .MILLI., .METRE. ) );
#10363=TOROIDAL_SURFACE ( 'NONE', #159107, 10.89999999999920455, 0.2000000000000000111 ) ;
#10558=COLOUR_RGB ( '', 0.40784314, 0.44705882, 0.49803922) ;
#11036=FACE_OUTER_BOUND ( 'NONE', #129823, .T. ) ;
#11059=ORIENTED_EDGE ( 'NONE', *, *, #119894, .F. ) ;
#12822=DIRECTION ( 'NONE',  ( -1.000000000000000000, 0.000000000000000000, 0.000000000000000000 ) ) ;
#13033=ORIENTED_EDGE ( 'NONE', *, *, #58125, .T. ) ;
#13610=( GEOMETRIC_REPRESENTATION_CONTEXT ( 3 ) GLOBAL_UNCERTAINTY_ASSIGNED_CONTEXT ( ( #36331 ) ) GLOBAL_UNIT_ASSIGNED_CONTEXT ( ( #9616, #189440, #72474 ) ) REPRESENTATION_CONTEXT ( 'NONE', 'WORKASPACE' ) );
#14175=SURFACE_SIDE_STYLE ('',( #49903 ) ) ;
#15009=MECHANICAL_DESIGN_GEOMETRIC_PRESENTATION_REPRESENTATION('',(#118843),#174174);
#15231=EDGE_CURVE ( 'NONE', #114534, #73830, #30756, .T. ) ;
#15427=CARTESIAN_POINT ( 'NONE',  ( 0.000000000000000000, 0.000000000000000000, 0.000000000000000000 ) ) ;
#17754=AXIS2_PLACEMENT_3D ( 'NONE', #134311, #187281, #38907 ) ;
#18139=MANIFOLD_SOLID_BREP ( 'Fillet1', #25706 ) ;
#18257=UNCERTAINTY_MEASURE_WITH_UNIT (LENGTH_MEASURE( 1.000000000000000082E-05 ), #42147, 'distance_accuracy_value', 'NONE');
#18418=CARTESIAN_POINT ( 'NONE',  ( 3.649297074908570321E-15, -6.789018801444764277E-15, 0.2598076211376221800 ) ) ;
#18899=ORIENTED_EDGE ( 'NONE', *, *, #157376, .F. ) ;
#19771=ORIENTED_EDGE ( 'NONE', *, *, #140437, .F. ) ;
#20228=ORIENTED_EDGE ( 'NONE', *, *, #127295, .F. ) ;
#20973=CARTESIAN_POINT ( 'NONE',  ( 11.09999999999960529, -3.437048488108780511E-15, -0.2598076211376266764 ) ) ;
#21037=PRODUCT_DEFINITION_FORMATION_WITH_SPECIFIED_SOURCE ( 'ANY', '', #74733, .NOT_KNOWN. ) ;
#22235=CIRCLE ( 'NONE', #171004, 11.09999999999999964 ) ;
#22632=EDGE_CURVE ( 'NONE', #74610, #143389, #61964, .T. ) ;
#22639=VECTOR ( 'NONE', #140517, 1000.000000000000000 ) ;
#22675=CARTESIAN_POINT ( 'NONE',  ( 3.649297074908570321E-15, -6.789018801444764277E-15, 0.2598076211376221800 ) ) ;
#22698=CARTESIAN_POINT ( 'NONE',  ( -10.75000000000000000, 0.000000000000000000, 0.000000000000000000 ) ) ;
#23981=CARTESIAN_POINT ( 'NONE',  ( 10.99999999999731060, 1.347111479061759252E-15, -0.4330127018938151884 ) ) ;
#24030=CARTESIAN_POINT ( 'NONE',  ( -10.24999999999999822, 0.000000000000000000, 6.123233995736778362E-17 ) ) ;
#24089=( LENGTH_UNIT ( ) NAMED_UNIT ( * ) SI_UNIT ( .MILLI., .METRE. ) );
#24575=CARTESIAN_POINT ( 'NONE',  ( 2.364109784339328312E-15, 11.09999999999999609, -5.500000000000003553 ) ) ;
#24794=DIRECTION ( 'NONE',  ( -0.000000000000000000, -0.000000000000000000, -1.000000000000000000 ) ) ;
#24934=AXIS2_PLACEMENT_3D ( 'NONE', #135653, #43504, #58661 ) ;
#25042=CARTESIAN_POINT ( 'NONE',  ( -6.760415694342130179E-18, -5.633679745285109895E-18, -0.4330127018938150774 ) ) ;
#25627=VERTEX_POINT ( 'NONE', #162197 ) ;
#25645=CARTESIAN_POINT ( 'NONE',  ( 11.09999999999960707, -2.070930125360890341E-15, 0.2598076211376220135 ) ) ;
#25706=CLOSED_SHELL ( 'NONE', ( #152368, #37246, #160190, #54459, #73787, #9068, #152261, #169109, #51527, #213750 ) ) ;
#25860=FILL_AREA_STYLE_COLOUR ( '', #6648 ) ;
#26228=PRESENTATION_STYLE_ASSIGNMENT (( #209227 ) ) ;
#27141=SURFACE_STYLE_FILL_AREA ( #191768 ) ;
#27270=SURFACE_STYLE_FILL_AREA ( #212406 ) ;
#27725=ORIENTED_EDGE ( 'NONE', *, *, #209210, .T. ) ;
#28003=( NAMED_UNIT ( * ) SI_UNIT ( $, .STERADIAN. ) SOLID_ANGLE_UNIT ( ) );
#28395=ORIENTED_EDGE ( 'NONE', *, *, #212736, .F. ) ;
#28502=TOROIDAL_SURFACE ( 'NONE', #163318, 10.89999999999920632, 0.2000000000000000111 ) ;
#28658=AXIS2_PLACEMENT_3D ( 'NONE', #22698, #88810, #157013 ) ;
#29102=DIRECTION ( 'NONE',  ( 1.224646799147353207E-16, 1.000000000000000000, -1.301042606982605629E-17 ) ) ;
#29148=DIRECTION ( 'NONE',  ( 2.031254238220912814E-34, -1.000000000000000000, 1.301042606982605475E-17 ) ) ;
#29459=ORIENTED_EDGE ( 'NONE', *, *, #166273, .F. ) ;
#29965=UNCERTAINTY_MEASURE_WITH_UNIT (LENGTH_MEASURE( 1.000000000000000082E-05 ), #78184, 'distance_accuracy_value', 'NONE');
#30698=STYLED_ITEM ( 'NONE', ( #197207 ), #213750 ) ;
#30756=CIRCLE ( 'NONE', #65342, 10.24999999999999822 ) ;
#31461=CIRCLE ( 'NONE', #48776, 0.2000000000000000389 ) ;
#31559=SURFACE_SIDE_STYLE ('',( #27270 ) ) ;
#31713=SURFACE_SIDE_STYLE ('',( #184330 ) ) ;
#32251=ORIENTED_EDGE ( 'NONE', *, *, #198010, .T. ) ;
#32746=AXIS2_PLACEMENT_3D ( 'NONE', #18418, #83423, #33615 ) ;
#33475=AXIS2_PLACEMENT_3D ( 'NONE', #83487, #118197, #151715 ) ;
#33615=DIRECTION ( 'NONE',  ( -1.000000000000000000, 0.000000000000000000, 1.465138070926357285E-17 ) ) ;
#33893=DIRECTION ( 'NONE',  ( -1.000000000000000000, 0.000000000000000000, 1.478457507935137263E-17 ) ) ;
#33984=( GEOMETRIC_REPRESENTATION_CONTEXT ( 3 ) GLOBAL_UNCERTAINTY_ASSIGNED_CONTEXT ( ( #926 ) ) GLOBAL_UNIT_ASSIGNED_CONTEXT ( ( #6639, #40240, #152914 ) ) REPRESENTATION_CONTEXT ( 'NONE', 'WORKASPACE' ) );
#34716=CARTESIAN_POINT ( 'NONE',  ( 10.75000000000000000, 1.316495309083404618E-15, 0.000000000000000000 ) ) ;
#34949=DIRECTION ( 'NONE',  ( 1.561251128379126077E-17, 1.301042606982605475E-17, 1.000000000000000000 ) ) ;
#36331=UNCERTAINTY_MEASURE_WITH_UNIT (LENGTH_MEASURE( 1.000000000000000082E-05 ), #9616, 'distance_accuracy_value', 'NONE');
#36396=CARTESIAN_POINT ( 'NONE',  ( 10.89999999999920810, -2.095423061343886359E-15, 0.2598076211376220135 ) ) ;
#36747=ORIENTED_EDGE ( 'NONE', *, *, #49562, .T. ) ;
#36868=CIRCLE ( 'NONE', #33475, 0.2000000000000000111 ) ;
#37061=CARTESIAN_POINT ( 'NONE',  ( 3.633072077242065861E-15, -6.802539632833518519E-15, -0.2598076211376265099 ) ) ;
#37246=ADVANCED_FACE ( 'NONE', ( #38929 ), #68479, .T. ) ;
#38907=DIRECTION ( 'NONE',  ( -1.000000000000000000, -1.224646799147353454E-16, 0.000000000000000000 ) ) ;
#38929=FACE_OUTER_BOUND ( 'NONE', #211277, .T. ) ;
#40230=ORIENTED_EDGE ( 'NONE', *, *, #159606, .F. ) ;
#40240=( NAMED_UNIT ( * ) PLANE_ANGLE_UNIT ( ) SI_UNIT ( $, .RADIAN. ) );
#40375=FILL_AREA_STYLE ('',( #141104 ) ) ;
#41358=DIRECTION ( 'NONE',  ( -1.000000000000000000, 0.000000000000000000, 1.465138070926357285E-17 ) ) ;
#41483=( GEOMETRIC_REPRESENTATION_CONTEXT ( 3 ) GLOBAL_UNCERTAINTY_ASSIGNED_CONTEXT ( ( #18257 ) ) GLOBAL_UNIT_ASSIGNED_CONTEXT ( ( #42147, #125592, #28003 ) ) REPRESENTATION_CONTEXT ( 'NONE', 'WORKASPACE' ) );
#41899=PRODUCT_DEFINITION_SHAPE ( 'NONE', 'NONE',  #196048 ) ;
#42147=( LENGTH_UNIT ( ) NAMED_UNIT ( * ) SI_UNIT ( .MILLI., .METRE. ) );
#42288=COLOUR_RGB ( '', 0.40784314, 0.44705882, 0.49803922) ;
#42519=FILL_AREA_STYLE ('',( #190858 ) ) ;
#43218=PRESENTATION_STYLE_ASSIGNMENT (( #174285 ) ) ;
#43504=DIRECTION ( 'NONE',  ( 1.561251128379126077E-17, 1.301042606982605475E-17, 1.000000000000000000 ) ) ;
#44351=EDGE_LOOP ( 'NONE', ( #161068, #92613, #74337, #163655 ) ) ;
#45689=( LENGTH_UNIT ( ) NAMED_UNIT ( * ) SI_UNIT ( .MILLI., .METRE. ) );
#45842=AXIS2_PLACEMENT_3D ( 'NONE', #36396, #69941, #122011 ) ;
#48180=( GEOMETRIC_REPRESENTATION_CONTEXT ( 3 ) GLOBAL_UNCERTAINTY_ASSIGNED_CONTEXT ( ( #167689 ) ) GLOBAL_UNIT_ASSIGNED_CONTEXT ( ( #213440, #161538, #179911 ) ) REPRESENTATION_CONTEXT ( 'NONE', 'WORKASPACE' ) );
#48776=AXIS2_PLACEMENT_3D ( 'NONE', #148240, #29148, #132021 ) ;
#48779=EDGE_LOOP ( 'NONE', ( #11059, #29459, #135432, #213429 ) ) ;
#48847=FACE_OUTER_BOUND ( 'NONE', #160446, .T. ) ;
#49029=( NAMED_UNIT ( * ) PLANE_ANGLE_UNIT ( ) SI_UNIT ( $, .RADIAN. ) );
#49562=EDGE_CURVE ( 'NONE', #143389, #204176, #166727, .T. ) ;
#49903=SURFACE_STYLE_FILL_AREA ( #129115 ) ;
#50402=AXIS2_PLACEMENT_3D ( 'NONE', #137781, #72751, #41358 ) ;
#51527=ADVANCED_FACE ( 'NONE', ( #111912 ), #28502, .T. ) ;
#51765=VERTEX_POINT ( 'NONE', #67309 ) ;
#52148=DIRECTION ( 'NONE',  ( 2.220446049250312341E-16, -1.000000000000000000, 0.000000000000000000 ) ) ;
#52153=EDGE_CURVE ( 'NONE', #195274, #191668, #139215, .T. ) ;
#52216=SURFACE_STYLE_USAGE ( .BOTH. , #200570 ) ;
#52289=ORIENTED_EDGE ( 'NONE', *, *, #22632, .T. ) ;
#53065=TOROIDAL_SURFACE ( 'NONE', #70209, 10.89999999999920632, 0.2000000000000000111 ) ;
#54285=DIRECTION ( 'NONE',  ( 3.122502256758252154E-17, 2.602085213965210950E-17, 1.000000000000000000 ) ) ;
#54459=ADVANCED_FACE ( 'NONE', ( #144152 ), #53065, .T. ) ;
#54753=EDGE_CURVE ( 'NONE', #95626, #186548, #201783, .T. ) ;
#56037=CARTESIAN_POINT ( 'NONE',  ( -11.09999999999959996, -2.077690541055267462E-15, -0.2598076211376263434 ) ) ;
#57311=SURFACE_STYLE_USAGE ( .BOTH. , #175343 ) ;
#57524=( NAMED_UNIT ( * ) PLANE_ANGLE_UNIT ( ) SI_UNIT ( $, .RADIAN. ) );
#57738=( GEOMETRIC_REPRESENTATION_CONTEXT ( 3 ) GLOBAL_UNCERTAINTY_ASSIGNED_CONTEXT ( ( #101339 ) ) GLOBAL_UNIT_ASSIGNED_CONTEXT ( ( #45689, #65088, #185235 ) ) REPRESENTATION_CONTEXT ( 'NONE', 'WORKASPACE' ) );
#58125=EDGE_CURVE ( 'NONE', #186548, #74610, #31461, .T. ) ;
#58352=CIRCLE ( 'NONE', #207080, 11.09999999999999964 ) ;
#58575=AXIS2_PLACEMENT_3D ( 'NONE', #115018, #177837, #129170 ) ;
#58661=DIRECTION ( 'NONE',  ( 1.000000000000000000, 0.000000000000000000, -1.465138070926357285E-17 ) ) ;
#60765=CIRCLE ( 'NONE', #1814, 10.99999999999733369 ) ;
#61316=AXIS2_PLACEMENT_3D ( 'NONE', #179619, #29102, #163372 ) ;
#61964=CIRCLE ( 'NONE', #134650, 11.09999999999999964 ) ;
#62026=( NAMED_UNIT ( * ) PLANE_ANGLE_UNIT ( ) SI_UNIT ( $, .RADIAN. ) );
#62987=ORIENTED_EDGE ( 'NONE', *, *, #180163, .F. ) ;
#63910=CARTESIAN_POINT ( 'NONE',  ( 1.781714131423858791E-15, -3.430288072414404179E-15, 0.2598076211376221800 ) ) ;
#64532=STYLED_ITEM ( 'NONE', ( #196186 ), #18139 ) ;
#65063=DIRECTION ( 'NONE',  ( 1.561251128379126077E-17, 1.301042606982605475E-17, 1.000000000000000000 ) ) ;
#65088=( NAMED_UNIT ( * ) PLANE_ANGLE_UNIT ( ) SI_UNIT ( $, .RADIAN. ) );
#65342=AXIS2_PLACEMENT_3D ( 'NONE', #97491, #132142, #200274 ) ;
#65502=EDGE_CURVE ( 'NONE', #114534, #25627, #167039, .T. ) ;
#67206=CARTESIAN_POINT ( 'NONE',  ( -6.760415694342130179E-18, -5.633679745285109895E-18, -0.4330127018938150774 ) ) ;
#67309=CARTESIAN_POINT ( 'NONE',  ( 2.535847408461032609E-15, 11.09999999999999432, 0.2598076211376220135 ) ) ;
#67327=ORIENTED_EDGE ( 'NONE', *, *, #130606, .T. ) ;
#67359=( NAMED_UNIT ( * ) SI_UNIT ( $, .STERADIAN. ) SOLID_ANGLE_UNIT ( ) );
#67798=DIRECTION ( 'NONE',  ( 1.561251128379126077E-17, 1.301042606982605475E-17, 1.000000000000000000 ) ) ;
#68479=TOROIDAL_SURFACE ( 'NONE', #68935, 10.75000000000000000, 0.5000000000000007772 ) ;
#68935=AXIS2_PLACEMENT_3D ( 'NONE', #141804, #24794, #106114 ) ;
#69305=ORIENTED_EDGE ( 'NONE', *, *, #198010, .F. ) ;
#69504=CARTESIAN_POINT ( 'NONE',  ( 0.000000000000000000, 0.000000000000000000, 0.000000000000000000 ) ) ;
#69941=DIRECTION ( 'NONE',  ( -1.224646799147353207E-16, 1.000000000000000000, -1.301042606982605321E-17 ) ) ;
#70209=AXIS2_PLACEMENT_3D ( 'NONE', #63910, #178747, #96447 ) ;
#71420=DIRECTION ( 'NONE',  ( 1.561251128379126077E-17, 1.301042606982605475E-17, 1.000000000000000000 ) ) ;
#71467=DIRECTION ( 'NONE',  ( -1.224646799147353207E-16, 1.000000000000000000, 0.000000000000000000 ) ) ;
#71759=SHAPE_REPRESENTATION_RELATIONSHIP ( 'NONE' , 'NONE' ,  #189584, #166452 ) ;
#71984=AXIS2_PLACEMENT_3D ( 'NONE', #15427, #80451, #115147 ) ;
#72474=( NAMED_UNIT ( * ) SI_UNIT ( $, .STERADIAN. ) SOLID_ANGLE_UNIT ( ) );
#72751=DIRECTION ( 'NONE',  ( -1.561251128379126077E-17, -1.301042606982605475E-17, -1.000000000000000000 ) ) ;
#73553=SURFACE_STYLE_FILL_AREA ( #105012 ) ;
#73787=ADVANCED_FACE ( 'NONE', ( #3366 ), #101963, .T. ) ;
#73830=VERTEX_POINT ( 'NONE', #120422 ) ;
#73927=( NAMED_UNIT ( * ) PLANE_ANGLE_UNIT ( ) SI_UNIT ( $, .RADIAN. ) );
#74337=ORIENTED_EDGE ( 'NONE', *, *, #65502, .T. ) ;
#74499=DIRECTION ( 'NONE',  ( -1.561251128379126077E-17, -1.301042606982605475E-17, -1.000000000000000000 ) ) ;
#74610=VERTEX_POINT ( 'NONE', #20973 ) ;
#74733=PRODUCT ( 'rubber for base', 'rubber for base', '', ( #85090 ) ) ;
#75562=DIRECTION ( 'NONE',  ( -1.000000000000000000, 0.000000000000000000, 1.465138070926357285E-17 ) ) ;
#75825=MECHANICAL_DESIGN_GEOMETRIC_PRESENTATION_REPRESENTATION('',(#30698),#48180);
#76133=FILL_AREA_STYLE ('',( #161668 ) ) ;
#76187=EDGE_CURVE ( 'NONE', #95626, #114534, #111495, .T. ) ;
#76453=CARTESIAN_POINT ( 'NONE',  ( 5.934142066621461235E-15, -11.10000000000000853, -5.500000000000003553 ) ) ;
#77579=CARTESIAN_POINT ( 'NONE',  ( 6.760415694340460783E-18, 5.633679745283718603E-18, 0.4330127018937082184 ) ) ;
#78184=( LENGTH_UNIT ( ) NAMED_UNIT ( * ) SI_UNIT ( .MILLI., .METRE. ) );
#78487=CARTESIAN_POINT ( 'NONE',  ( -10.75000000000000000, 0.000000000000000000, 0.000000000000000000 ) ) ;
#79017=EDGE_LOOP ( 'NONE', ( #142319, #116679, #164190, #18899, #20228 ) ) ;
#79334=SURFACE_STYLE_FILL_AREA ( #76133 ) ;
#79484=MECHANICAL_DESIGN_GEOMETRIC_PRESENTATION_REPRESENTATION('',(#134861),#41483);
#80451=DIRECTION ( 'NONE',  ( -0.000000000000000000, -0.000000000000000000, -1.000000000000000000 ) ) ;
#81273=CIRCLE ( 'NONE', #105564, 10.24999999999999822 ) ;
#81336=SURFACE_STYLE_USAGE ( .BOTH. , #14175 ) ;
#82876=COLOUR_RGB ( '', 0.40784314, 0.44705882, 0.49803922) ;
#83423=DIRECTION ( 'NONE',  ( -1.561251128379126077E-17, -1.301042606982605475E-17, -1.000000000000000000 ) ) ;
#83487=CARTESIAN_POINT ( 'NONE',  ( -10.89999999999920632, -3.430288072414404179E-15, 0.2598076211376223466 ) ) ;
#84712=FILL_AREA_STYLE ('',( #100950 ) ) ;
#85015=UNCERTAINTY_MEASURE_WITH_UNIT (LENGTH_MEASURE( 1.000000000000000082E-05 ), #24089, 'distance_accuracy_value', 'NONE');
#85090=PRODUCT_CONTEXT ( 'NONE', #86421, 'mechanical' ) ;
#85791=AXIS2_PLACEMENT_3D ( 'NONE', #69504, #104176, #137750 ) ;
#86064=ORIENTED_EDGE ( 'NONE', *, *, #15231, .F. ) ;
#86421=APPLICATION_CONTEXT ( 'automotive_design' ) ;
#86630=CARTESIAN_POINT ( 'NONE',  ( 6.760415694340460783E-18, 5.633679745283718603E-18, 0.4330127018937082184 ) ) ;
#86633=STYLED_ITEM ( 'NONE', ( #207115 ), #166452 ) ;
#87189=ORIENTED_EDGE ( 'NONE', *, *, #22632, .F. ) ;
#88810=DIRECTION ( 'NONE',  ( 0.000000000000000000, -1.000000000000000000, 0.000000000000000000 ) ) ;
#90741=AXIS2_PLACEMENT_3D ( 'NONE', #78487, #144604, #179205 ) ;
#90923=DIRECTION ( 'NONE',  ( -1.561251128379126077E-17, -1.301042606982605475E-17, -1.000000000000000000 ) ) ;
#90938=ORIENTED_EDGE ( 'NONE', *, *, #159606, .T. ) ;
#91109=FILL_AREA_STYLE_COLOUR ( '', #170563 ) ;
#91969=CARTESIAN_POINT ( 'NONE',  ( 1.773601632590606955E-15, -3.437048488108780906E-15, -0.2598076211376265099 ) ) ;
#92613=ORIENTED_EDGE ( 'NONE', *, *, #119894, .T. ) ;
#93032=SURFACE_STYLE_FILL_AREA ( #110393 ) ;
#93246=SURFACE_STYLE_USAGE ( .BOTH. , #210144 ) ;
#93320=DIRECTION ( 'NONE',  ( 1.000000000000000000, 0.000000000000000000, -1.465138070926357285E-17 ) ) ;
#94545=SURFACE_STYLE_USAGE ( .BOTH. , #129252 ) ;
#95216=CARTESIAN_POINT ( 'NONE',  ( 0.000000000000000000, 0.000000000000000000, 0.000000000000000000 ) ) ;
#95626=VERTEX_POINT ( 'NONE', #188253 ) ;
#96164=CIRCLE ( 'NONE', #102933, 11.09999999999999964 ) ;
#96447=DIRECTION ( 'NONE',  ( -1.000000000000000000, 1.250471828332832423E-35, 1.561251128379126077E-17 ) ) ;
#97491=CARTESIAN_POINT ( 'NONE',  ( 0.000000000000000000, 0.000000000000000000, 6.123233995736775897E-17 ) ) ;
#99548=MECHANICAL_DESIGN_GEOMETRIC_PRESENTATION_REPRESENTATION('',(#165247),#182403);
#99696=TOROIDAL_SURFACE ( 'NONE', #71984, 10.75000000000000000, 0.5000000000000007772 ) ;
#99730=DIRECTION ( 'NONE',  ( -1.000000000000000000, -1.224646799147353454E-16, 0.000000000000000000 ) ) ;
#100743=DIRECTION ( 'NONE',  ( -1.000000000000000000, 0.000000000000000000, 1.478457507935137263E-17 ) ) ;
#100757=AXIS2_PLACEMENT_3D ( 'NONE', #198374, #54285, #52148 ) ;
#100950=FILL_AREA_STYLE_COLOUR ( '', #165397 ) ;
#101339=UNCERTAINTY_MEASURE_WITH_UNIT (LENGTH_MEASURE( 1.000000000000000082E-05 ), #45689, 'distance_accuracy_value', 'NONE');
#101963=CYLINDRICAL_SURFACE ( 'NONE', #100757, 11.10000000000000142 ) ;
#102342=CIRCLE ( 'NONE', #50402, 11.09999999999999964 ) ;
#102933=AXIS2_PLACEMENT_3D ( 'NONE', #191423, #74499, #75562 ) ;
#103518=EDGE_CURVE ( 'NONE', #51765, #191668, #96164, .T. ) ;
#104176=DIRECTION ( 'NONE',  ( -0.000000000000000000, -0.000000000000000000, -1.000000000000000000 ) ) ;
#105012=FILL_AREA_STYLE ('',( #25860 ) ) ;
#105564=AXIS2_PLACEMENT_3D ( 'NONE', #195865, #127766, #12822 ) ;
#106114=DIRECTION ( 'NONE',  ( -1.000000000000000000, 0.000000000000000000, 0.000000000000000000 ) ) ;
#106477=SURFACE_STYLE_USAGE ( .BOTH. , #4616 ) ;
#107784=ORIENTED_EDGE ( 'NONE', *, *, #157376, .T. ) ;
#107869=ORIENTED_EDGE ( 'NONE', *, *, #209210, .F. ) ;
#108626=SURFACE_STYLE_FILL_AREA ( #42519 ) ;
#109102=DIRECTION ( 'NONE',  ( 1.561251128379126077E-17, 1.301042606982605475E-17, 1.000000000000000000 ) ) ;
#109678=FILL_AREA_STYLE_COLOUR ( '', #137215 ) ;
#110393=FILL_AREA_STYLE ('',( #191552 ) ) ;
#110833=DIRECTION ( 'NONE',  ( -1.000000000000000000, 1.250471828332832423E-35, 1.561251128379126077E-17 ) ) ;
#110923=AXIS2_PLACEMENT_3D ( 'NONE', #115452, #131686, #143673 ) ;
#111495=CIRCLE ( 'NONE', #90741, 0.5000000000000007772 ) ;
#111671=( LENGTH_UNIT ( ) NAMED_UNIT ( * ) SI_UNIT ( .MILLI., .METRE. ) );
#111912=FACE_OUTER_BOUND ( 'NONE', #171477, .T. ) ;
#112346=UNCERTAINTY_MEASURE_WITH_UNIT (LENGTH_MEASURE( 1.000000000000000082E-05 ), #145452, 'distance_accuracy_value', 'NONE');
#114534=VERTEX_POINT ( 'NONE', #24030 ) ;
#115018=CARTESIAN_POINT ( 'NONE',  ( 0.000000000000000000, 0.000000000000000000, 0.000000000000000000 ) ) ;
#115147=DIRECTION ( 'NONE',  ( -1.000000000000000000, 0.000000000000000000, 0.000000000000000000 ) ) ;
#115300=AXIS2_PLACEMENT_3D ( 'NONE', #25042, #125840, #206990 ) ;
#115452=CARTESIAN_POINT ( 'NONE',  ( 3.469446951953614189E-15, -6.938893903907228378E-15, -5.500000000000003553 ) ) ;
#115558=EDGE_CURVE ( 'NONE', #186548, #95626, #1459, .T. ) ;
#116025=CARTESIAN_POINT ( 'NONE',  ( 1.773601632590606955E-15, -3.437048488108780906E-15, -0.2598076211376265099 ) ) ;
#116679=ORIENTED_EDGE ( 'NONE', *, *, #52153, .T. ) ;
#117584=PRODUCT_DEFINITION_CONTEXT ( 'detailed design', #162660, 'design' ) ;
#118197=DIRECTION ( 'NONE',  ( 2.031254238220912814E-34, -1.000000000000000000, 1.301042606982605475E-17 ) ) ;
#118843=STYLED_ITEM ( 'NONE', ( #159280 ), #54459 ) ;
#119537=( NAMED_UNIT ( * ) SI_UNIT ( $, .STERADIAN. ) SOLID_ANGLE_UNIT ( ) );
#119894=EDGE_CURVE ( 'NONE', #73830, #114534, #81273, .T. ) ;
#120422=CARTESIAN_POINT ( 'NONE',  ( 10.24999999999999822, 1.255262969126037044E-15, 6.123233995736778362E-17 ) ) ;
#120534=ORIENTED_EDGE ( 'NONE', *, *, #52153, .F. ) ;
#120620=SURFACE_STYLE_FILL_AREA ( #40375 ) ;
#120962=TOROIDAL_SURFACE ( 'NONE', #58575, 10.75000000000000000, 0.5000000000000007772 ) ;
#121973=( GEOMETRIC_REPRESENTATION_CONTEXT ( 3 ) GLOBAL_UNCERTAINTY_ASSIGNED_CONTEXT ( ( #112346 ) ) GLOBAL_UNIT_ASSIGNED_CONTEXT ( ( #145452, #62026, #209304 ) ) REPRESENTATION_CONTEXT ( 'NONE', 'WORKASPACE' ) );
#122011=DIRECTION ( 'NONE',  ( -1.000000000000000000, -1.224646799147343593E-16, 0.000000000000000000 ) ) ;
#122659=AXIS2_PLACEMENT_3D ( 'NONE', #67206, #165810, #136522 ) ;
#124531=DIRECTION ( 'NONE',  ( 1.000000000000000000, -1.250471828332824404E-35, -1.561251128379126077E-17 ) ) ;
#125592=( NAMED_UNIT ( * ) PLANE_ANGLE_UNIT ( ) SI_UNIT ( $, .RADIAN. ) );
#125840=DIRECTION ( 'NONE',  ( -1.561251128379126077E-17, -1.301042606982605475E-17, -1.000000000000000000 ) ) ;
#126783=UNCERTAINTY_MEASURE_WITH_UNIT (LENGTH_MEASURE( 1.000000000000000082E-05 ), #1300, 'distance_accuracy_value', 'NONE');
#126905=ORIENTED_EDGE ( 'NONE', *, *, #212736, .T. ) ;
#127295=EDGE_CURVE ( 'NONE', #25627, #166389, #36868, .T. ) ;
#127324=TOROIDAL_SURFACE ( 'NONE', #85791, 10.75000000000000000, 0.5000000000000007772 ) ;
#127409=CIRCLE ( 'NONE', #151447, 11.09999999999999964 ) ;
#127470=CYLINDRICAL_SURFACE ( 'NONE', #110923, 11.10000000000000142 ) ;
#127766=DIRECTION ( 'NONE',  ( -0.000000000000000000, -0.000000000000000000, -1.000000000000000000 ) ) ;
#128265=ORIENTED_EDGE ( 'NONE', *, *, #127295, .T. ) ;
#129115=FILL_AREA_STYLE ('',( #164715 ) ) ;
#129170=DIRECTION ( 'NONE',  ( -1.000000000000000000, 0.000000000000000000, 0.000000000000000000 ) ) ;
#129252=SURFACE_SIDE_STYLE ('',( #79334 ) ) ;
#129823=EDGE_LOOP ( 'NONE', ( #86064, #201187, #179949, #173446 ) ) ;
#130348=FILL_AREA_STYLE_COLOUR ( '', #203262 ) ;
#130606=EDGE_CURVE ( 'NONE', #73830, #195274, #163567, .T. ) ;
#130687=CARTESIAN_POINT ( 'NONE',  ( 3.633072077242065861E-15, -6.802539632833518519E-15, -0.2598076211376265099 ) ) ;
#131686=DIRECTION ( 'NONE',  ( 3.122502256758252154E-17, 2.602085213965210950E-17, 1.000000000000000000 ) ) ;
#132002=DIRECTION ( 'NONE',  ( 0.000000000000000000, 0.000000000000000000, 1.000000000000000000 ) ) ;
#132021=DIRECTION ( 'NONE',  ( 0.000000000000000000, -1.301042606982654316E-17, -1.000000000000000000 ) ) ;
#132142=DIRECTION ( 'NONE',  ( -0.000000000000000000, -0.000000000000000000, -1.000000000000000000 ) ) ;
#132253=DIRECTION ( 'NONE',  ( 1.000000000000000000, -1.250471828332824404E-35, -1.561251128379126077E-17 ) ) ;
#133371=( NAMED_UNIT ( * ) SI_UNIT ( $, .STERADIAN. ) SOLID_ANGLE_UNIT ( ) );
#134311=CARTESIAN_POINT ( 'NONE',  ( 10.75000000000000000, 1.316495309083404618E-15, 0.000000000000000000 ) ) ;
#134569=SURFACE_STYLE_FILL_AREA ( #84712 ) ;
#134650=AXIS2_PLACEMENT_3D ( 'NONE', #152292, #67798, #664 ) ;
#134837=ORIENTED_EDGE ( 'NONE', *, *, #54753, .F. ) ;
#134861=STYLED_ITEM ( 'NONE', ( #173213 ), #160190 ) ;
#135432=ORIENTED_EDGE ( 'NONE', *, *, #115558, .T. ) ;
#135653=CARTESIAN_POINT ( 'NONE',  ( 3.633072077242065861E-15, -6.802539632833518519E-15, -0.2598076211376265099 ) ) ;
#136522=DIRECTION ( 'NONE',  ( 1.000000000000000000, 0.000000000000000000, -1.478457507935129867E-17 ) ) ;
#137215=COLOUR_RGB ( '', 0.40784314, 0.44705882, 0.49803922) ;
#137537=EDGE_CURVE ( 'NONE', #195274, #25627, #60765, .T. ) ;
#137750=DIRECTION ( 'NONE',  ( -1.000000000000000000, 0.000000000000000000, 0.000000000000000000 ) ) ;
#137759=MECHANICAL_DESIGN_GEOMETRIC_PRESENTATION_REPRESENTATION('',(#196501),#33984);
#137781=CARTESIAN_POINT ( 'NONE',  ( 3.649297074908570321E-15, -6.789018801444764277E-15, 0.2598076211376221800 ) ) ;
#138211=COLOUR_RGB ( '', 0.09019608, 0.27058824, 0.51372549) ;
#138598=( GEOMETRIC_REPRESENTATION_CONTEXT ( 3 ) GLOBAL_UNCERTAINTY_ASSIGNED_CONTEXT ( ( #167343 ) ) GLOBAL_UNIT_ASSIGNED_CONTEXT ( ( #171423, #73927, #6765 ) ) REPRESENTATION_CONTEXT ( 'NONE', 'WORKASPACE' ) );
#138812=ORIENTED_EDGE ( 'NONE', *, *, #103518, .T. ) ;
#139215=CIRCLE ( 'NONE', #45842, 0.2000000000000005107 ) ;
#140437=EDGE_CURVE ( 'NONE', #191668, #193155, #102342, .T. ) ;
#140517=DIRECTION ( 'NONE',  ( 3.122502256758252154E-17, 2.602085213965210950E-17, 1.000000000000000000 ) ) ;
#140973=ORIENTED_EDGE ( 'NONE', *, *, #210859, .F. ) ;
#141021=DIRECTION ( 'NONE',  ( 1.561251128379126077E-17, 1.301042606982605475E-17, 1.000000000000000000 ) ) ;
#141104=FILL_AREA_STYLE_COLOUR ( '', #10558 ) ;
#141582=TOROIDAL_SURFACE ( 'NONE', #169207, 10.89999999999920455, 0.2000000000000000111 ) ;
#141587=ORIENTED_EDGE ( 'NONE', *, *, #191657, .F. ) ;
#141804=CARTESIAN_POINT ( 'NONE',  ( 0.000000000000000000, 0.000000000000000000, 0.000000000000000000 ) ) ;
#142236=PRESENTATION_STYLE_ASSIGNMENT (( #94545 ) ) ;
#142319=ORIENTED_EDGE ( 'NONE', *, *, #137537, .F. ) ;
#142450=CIRCLE ( 'NONE', #17754, 0.5000000000000004441 ) ;
#142749=ORIENTED_EDGE ( 'NONE', *, *, #58125, .F. ) ;
#143389=VERTEX_POINT ( 'NONE', #583 ) ;
#143673=DIRECTION ( 'NONE',  ( 2.220446049250312341E-16, -1.000000000000000000, 0.000000000000000000 ) ) ;
#144152=FACE_OUTER_BOUND ( 'NONE', #79017, .T. ) ;
#144604=DIRECTION ( 'NONE',  ( 0.000000000000000000, -1.000000000000000000, 0.000000000000000000 ) ) ;
#145452=( LENGTH_UNIT ( ) NAMED_UNIT ( * ) SI_UNIT ( .MILLI., .METRE. ) );
#148240=CARTESIAN_POINT ( 'NONE',  ( 10.89999999999920632, -3.437048488108780906E-15, -0.2598076211376266764 ) ) ;
#148657=FACE_OUTER_BOUND ( 'NONE', #48779, .T. ) ;
#148944=( GEOMETRIC_REPRESENTATION_CONTEXT ( 3 ) GLOBAL_UNCERTAINTY_ASSIGNED_CONTEXT ( ( #85015 ) ) GLOBAL_UNIT_ASSIGNED_CONTEXT ( ( #24089, #7837, #119537 ) ) REPRESENTATION_CONTEXT ( 'NONE', 'WORKASPACE' ) );
#150230=ORIENTED_EDGE ( 'NONE', *, *, #49562, .F. ) ;
#150799=FILL_AREA_STYLE ('',( #130348 ) ) ;
#151321=ORIENTED_EDGE ( 'NONE', *, *, #115558, .F. ) ;
#151447=AXIS2_PLACEMENT_3D ( 'NONE', #37061, #141021, #93320 ) ;
#151715=DIRECTION ( 'NONE',  ( 0.000000000000000000, -1.301042606982654625E-17, -1.000000000000000000 ) ) ;
#152011=MECHANICAL_DESIGN_GEOMETRIC_PRESENTATION_REPRESENTATION('',(#162368),#13610);
#152261=ADVANCED_FACE ( 'NONE', ( #148657 ), #99696, .T. ) ;
#152292=CARTESIAN_POINT ( 'NONE',  ( 3.633072077242065861E-15, -6.802539632833518519E-15, -0.2598076211376265099 ) ) ;
#152368=ADVANCED_FACE ( 'NONE', ( #183273 ), #127324, .T. ) ;
#152914=( NAMED_UNIT ( * ) SI_UNIT ( $, .STERADIAN. ) SOLID_ANGLE_UNIT ( ) );
#153186=AXIS2_PLACEMENT_3D ( 'NONE', #34716, #71467, #99730 ) ;
#153870=ORIENTED_EDGE ( 'NONE', *, *, #15231, .T. ) ;
#154709=CIRCLE ( 'NONE', #61316, 0.2000000000000005107 ) ;
#154822=ORIENTED_EDGE ( 'NONE', *, *, #137537, .T. ) ;
#155517=( GEOMETRIC_REPRESENTATION_CONTEXT ( 3 ) GLOBAL_UNCERTAINTY_ASSIGNED_CONTEXT ( ( #29965 ) ) GLOBAL_UNIT_ASSIGNED_CONTEXT ( ( #78184, #160508, #133371 ) ) REPRESENTATION_CONTEXT ( 'NONE', 'WORKASPACE' ) );
#157013=DIRECTION ( 'NONE',  ( 0.000000000000000000, 0.000000000000000000, -1.000000000000000000 ) ) ;
#157195=VERTEX_POINT ( 'NONE', #183066 ) ;
#157376=EDGE_CURVE ( 'NONE', #166389, #51765, #22235, .T. ) ;
#158026=DIRECTION ( 'NONE',  ( 1.561251128379126077E-17, 1.301042606982605475E-17, 1.000000000000000000 ) ) ;
#158056=DIRECTION ( 'NONE',  ( -1.000000000000000000, 0.000000000000000000, 1.465138070926357285E-17 ) ) ;
#159107=AXIS2_PLACEMENT_3D ( 'NONE', #91969, #158026, #124531 ) ;
#159280=PRESENTATION_STYLE_ASSIGNMENT (( #93246 ) ) ;
#159516=CARTESIAN_POINT ( 'NONE',  ( 1.781714131423858791E-15, -3.430288072414404179E-15, 0.2598076211376221800 ) ) ;
#159606=EDGE_CURVE ( 'NONE', #157195, #193155, #163059, .T. ) ;
#160190=ADVANCED_FACE ( 'NONE', ( #192619 ), #10363, .T. ) ;
#160446=EDGE_LOOP ( 'NONE', ( #69305, #151321, #13033, #28395, #107869 ) ) ;
#160508=( NAMED_UNIT ( * ) PLANE_ANGLE_UNIT ( ) SI_UNIT ( $, .RADIAN. ) );
#161068=ORIENTED_EDGE ( 'NONE', *, *, #130606, .F. ) ;
#161266=DIRECTION ( 'NONE',  ( 1.000000000000000000, 0.000000000000000000, 0.000000000000000000 ) ) ;
#161538=( NAMED_UNIT ( * ) PLANE_ANGLE_UNIT ( ) SI_UNIT ( $, .RADIAN. ) );
#161565=SURFACE_STYLE_USAGE ( .BOTH. , #31559 ) ;
#161668=FILL_AREA_STYLE_COLOUR ( '', #42288 ) ;
#162119=COLOUR_RGB ( '', 0.09019608, 0.27058824, 0.51372549) ;
#162197=CARTESIAN_POINT ( 'NONE',  ( -10.99999999999737632, 0.000000000000000000, 0.4330127018937083849 ) ) ;
#162368=STYLED_ITEM ( 'NONE', ( #43218 ), #37246 ) ;
#162382=ORIENTED_EDGE ( 'NONE', *, *, #140437, .T. ) ;
#162660=APPLICATION_CONTEXT ( 'automotive_design' ) ;
#163059=LINE ( 'NONE', #76453, #210900 ) ;
#163318=AXIS2_PLACEMENT_3D ( 'NONE', #159516, #174731, #110833 ) ;
#163372=DIRECTION ( 'NONE',  ( -1.000000000000000000, 1.224646799147343593E-16, 0.000000000000000000 ) ) ;
#163567=CIRCLE ( 'NONE', #153186, 0.5000000000000004441 ) ;
#163655=ORIENTED_EDGE ( 'NONE', *, *, #210859, .T. ) ;
#164036=EDGE_LOOP ( 'NONE', ( #134837, #32251, #150230, #87189, #142749 ) ) ;
#164190=ORIENTED_EDGE ( 'NONE', *, *, #103518, .F. ) ;
#164715=FILL_AREA_STYLE_COLOUR ( '', #162119 ) ;
#164879=MECHANICAL_DESIGN_GEOMETRIC_PRESENTATION_REPRESENTATION('',(#64532),#57738);
#165247=STYLED_ITEM ( 'NONE', ( #181144 ), #152261 ) ;
#165397=COLOUR_RGB ( '', 0.31764706, 0.68627451, 0.89019608) ;
#165810=DIRECTION ( 'NONE',  ( -1.561251128379126077E-17, -1.301042606982605475E-17, -1.000000000000000000 ) ) ;
#166273=EDGE_CURVE ( 'NONE', #186548, #73830, #142450, .T. ) ;
#166389=VERTEX_POINT ( 'NONE', #192595 ) ;
#166452=ADVANCED_BREP_SHAPE_REPRESENTATION ( '', ( #18139, #200407 ), #138598 ) ;
#166727=CIRCLE ( 'NONE', #24934, 11.09999999999999964 ) ;
#167039=CIRCLE ( 'NONE', #28658, 0.5000000000000007772 ) ;
#167343=UNCERTAINTY_MEASURE_WITH_UNIT (LENGTH_MEASURE( 1.000000000000000082E-05 ), #171423, 'distance_accuracy_value', 'NONE');
#167689=UNCERTAINTY_MEASURE_WITH_UNIT (LENGTH_MEASURE( 1.000000000000000082E-05 ), #213440, 'distance_accuracy_value', 'NONE');
#169109=ADVANCED_FACE ( 'NONE', ( #178274 ), #127470, .T. ) ;
#169125=ORIENTED_EDGE ( 'NONE', *, *, #180163, .T. ) ;
#169207=AXIS2_PLACEMENT_3D ( 'NONE', #116025, #65063, #132253 ) ;
#170563=COLOUR_RGB ( '', 0.66274510, 0.83137255, 0.94901961) ;
#171004=AXIS2_PLACEMENT_3D ( 'NONE', #22675, #90923, #158056 ) ;
#171423=( LENGTH_UNIT ( ) NAMED_UNIT ( * ) SI_UNIT ( .MILLI., .METRE. ) );
#171477=EDGE_LOOP ( 'NONE', ( #120534, #140973, #128265, #62987, #19771 ) ) ;
#172473=AXIS2_PLACEMENT_3D ( 'NONE', #86630, #71420, #100743 ) ;
#173213=PRESENTATION_STYLE_ASSIGNMENT (( #57311 ) ) ;
#173446=ORIENTED_EDGE ( 'NONE', *, *, #166273, .T. ) ;
#173868=MECHANICAL_DESIGN_GEOMETRIC_PRESENTATION_REPRESENTATION('',(#187588),#121973);
#174174=( GEOMETRIC_REPRESENTATION_CONTEXT ( 3 ) GLOBAL_UNCERTAINTY_ASSIGNED_CONTEXT ( ( #195144 ) ) GLOBAL_UNIT_ASSIGNED_CONTEXT ( ( #111671, #57524, #179805 ) ) REPRESENTATION_CONTEXT ( 'NONE', 'WORKASPACE' ) );
#174285=SURFACE_STYLE_USAGE ( .BOTH. , #203528 ) ;
#174654=SURFACE_SIDE_STYLE ('',( #108626 ) ) ;
#174731=DIRECTION ( 'NONE',  ( -1.561251128379126077E-17, -1.301042606982605475E-17, -1.000000000000000000 ) ) ;
#175343=SURFACE_SIDE_STYLE ('',( #93032 ) ) ;
#177837=DIRECTION ( 'NONE',  ( -0.000000000000000000, -0.000000000000000000, -1.000000000000000000 ) ) ;
#178274=FACE_OUTER_BOUND ( 'NONE', #9076, .T. ) ;
#178747=DIRECTION ( 'NONE',  ( -1.561251128379126077E-17, -1.301042606982605475E-17, -1.000000000000000000 ) ) ;
#179205=DIRECTION ( 'NONE',  ( 0.000000000000000000, 0.000000000000000000, -1.000000000000000000 ) ) ;
#179619=CARTESIAN_POINT ( 'NONE',  ( -10.89999999999920277, -2.102183477038263480E-15, -0.2598076211376263434 ) ) ;
#179805=( NAMED_UNIT ( * ) SI_UNIT ( $, .STERADIAN. ) SOLID_ANGLE_UNIT ( ) );
#179911=( NAMED_UNIT ( * ) SI_UNIT ( $, .STERADIAN. ) SOLID_ANGLE_UNIT ( ) );
#179949=ORIENTED_EDGE ( 'NONE', *, *, #54753, .T. ) ;
#180163=EDGE_CURVE ( 'NONE', #193155, #166389, #195257, .T. ) ;
#181144=PRESENTATION_STYLE_ASSIGNMENT (( #224 ) ) ;
#182403=( GEOMETRIC_REPRESENTATION_CONTEXT ( 3 ) GLOBAL_UNCERTAINTY_ASSIGNED_CONTEXT ( ( #126783 ) ) GLOBAL_UNIT_ASSIGNED_CONTEXT ( ( #1300, #49029, #67359 ) ) REPRESENTATION_CONTEXT ( 'NONE', 'WORKASPACE' ) );
#182801=CIRCLE ( 'NONE', #172473, 10.99999999999733369 ) ;
#183066=CARTESIAN_POINT ( 'NONE',  ( 6.105879690743165926E-15, -11.10000000000000675, -0.2598076211376263434 ) ) ;
#183273=FACE_OUTER_BOUND ( 'NONE', #44351, .T. ) ;
#184330=SURFACE_STYLE_FILL_AREA ( #150799 ) ;
#185235=( NAMED_UNIT ( * ) SI_UNIT ( $, .STERADIAN. ) SOLID_ANGLE_UNIT ( ) );
#186246=ORIENTED_EDGE ( 'NONE', *, *, #65502, .F. ) ;
#186548=VERTEX_POINT ( 'NONE', #23981 ) ;
#187281=DIRECTION ( 'NONE',  ( -1.224646799147353207E-16, 1.000000000000000000, 0.000000000000000000 ) ) ;
#187588=STYLED_ITEM ( 'NONE', ( #142236 ), #51527 ) ;
#187859=CARTESIAN_POINT ( 'NONE',  ( 10.99999999999737632, 1.347111479061767535E-15, 0.4330127018937080519 ) ) ;
#188253=CARTESIAN_POINT ( 'NONE',  ( -10.99999999999731237, 3.761581922631320025E-34, -0.4330127018938148553 ) ) ;
#189440=( NAMED_UNIT ( * ) PLANE_ANGLE_UNIT ( ) SI_UNIT ( $, .RADIAN. ) );
#189584=SHAPE_REPRESENTATION ( 'rubber for base', ( #200407 ), #138598 ) ;
#190858=FILL_AREA_STYLE_COLOUR ( '', #138211 ) ;
#191423=CARTESIAN_POINT ( 'NONE',  ( 3.649297074908570321E-15, -6.789018801444764277E-15, 0.2598076211376221800 ) ) ;
#191552=FILL_AREA_STYLE_COLOUR ( '', #82876 ) ;
#191657=EDGE_CURVE ( 'NONE', #143389, #51765, #208654, .T. ) ;
#191668=VERTEX_POINT ( 'NONE', #25645 ) ;
#191768=FILL_AREA_STYLE ('',( #91109 ) ) ;
#192595=CARTESIAN_POINT ( 'NONE',  ( -11.09999999999960174, -3.430288072414404179E-15, 0.2598076211376223466 ) ) ;
#192619=FACE_OUTER_BOUND ( 'NONE', #164036, .T. ) ;
#193155=VERTEX_POINT ( 'NONE', #211422 ) ;
#195144=UNCERTAINTY_MEASURE_WITH_UNIT (LENGTH_MEASURE( 1.000000000000000082E-05 ), #111671, 'distance_accuracy_value', 'NONE');
#195257=CIRCLE ( 'NONE', #32746, 11.09999999999999964 ) ;
#195274=VERTEX_POINT ( 'NONE', #187859 ) ;
#195865=CARTESIAN_POINT ( 'NONE',  ( 0.000000000000000000, 0.000000000000000000, 6.123233995736775897E-17 ) ) ;
#196048=PRODUCT_DEFINITION ( 'UNKNOWN', '', #21037, #117584 ) ;
#196186=PRESENTATION_STYLE_ASSIGNMENT (( #161565 ) ) ;
#196501=STYLED_ITEM ( 'NONE', ( #212568 ), #152368 ) ;
#196677=DIRECTION ( 'NONE',  ( 1.000000000000000000, 0.000000000000000000, -1.465138070926357285E-17 ) ) ;
#197207=PRESENTATION_STYLE_ASSIGNMENT (( #81336 ) ) ;
#198010=EDGE_CURVE ( 'NONE', #95626, #204176, #154709, .T. ) ;
#198374=CARTESIAN_POINT ( 'NONE',  ( 3.469446951953614189E-15, -6.938893903907228378E-15, -5.500000000000003553 ) ) ;
#199892=SHAPE_DEFINITION_REPRESENTATION ( #41899, #189584 ) ;
#200274=DIRECTION ( 'NONE',  ( -1.000000000000000000, 0.000000000000000000, 0.000000000000000000 ) ) ;
#200407=AXIS2_PLACEMENT_3D ( 'NONE', #95216, #132002, #161266 ) ;
#200482=MECHANICAL_DESIGN_GEOMETRIC_PRESENTATION_REPRESENTATION('',(#203879),#155517);
#200570=SURFACE_SIDE_STYLE ('',( #134569 ) ) ;
#201187=ORIENTED_EDGE ( 'NONE', *, *, #76187, .F. ) ;
#201783=CIRCLE ( 'NONE', #115300, 10.99999999999738698 ) ;
#203262=COLOUR_RGB ( '', 0.09019608, 0.27058824, 0.51372549) ;
#203528=SURFACE_SIDE_STYLE ('',( #73553 ) ) ;
#203772=EDGE_LOOP ( 'NONE', ( #126905, #52289, #8567, #138812, #162382, #40230 ) ) ;
#203879=STYLED_ITEM ( 'NONE', ( #26228 ), #9068 ) ;
#204176=VERTEX_POINT ( 'NONE', #56037 ) ;
#206990=DIRECTION ( 'NONE',  ( 1.000000000000000000, 0.000000000000000000, -1.478457507935129867E-17 ) ) ;
#207080=AXIS2_PLACEMENT_3D ( 'NONE', #130687, #109102, #196677 ) ;
#207115=PRESENTATION_STYLE_ASSIGNMENT (( #106477 ) ) ;
#207700=MECHANICAL_DESIGN_GEOMETRIC_PRESENTATION_REPRESENTATION('',(#86633),#148944);
#208654=LINE ( 'NONE', #24575, #22639 ) ;
#209210=EDGE_CURVE ( 'NONE', #204176, #157195, #127409, .T. ) ;
#209227=SURFACE_STYLE_USAGE ( .BOTH. , #174654 ) ;
#209304=( NAMED_UNIT ( * ) SI_UNIT ( $, .STERADIAN. ) SOLID_ANGLE_UNIT ( ) );
#210144=SURFACE_SIDE_STYLE ('',( #27141 ) ) ;
#210859=EDGE_CURVE ( 'NONE', #25627, #195274, #182801, .T. ) ;
#210900=VECTOR ( 'NONE', #212843, 1000.000000000000000 ) ;
#211277=EDGE_LOOP ( 'NONE', ( #186246, #153870, #67327, #154822 ) ) ;
#211422=CARTESIAN_POINT ( 'NONE',  ( 6.105879690743165926E-15, -11.10000000000000675, 0.2598076211376223466 ) ) ;
#212406=FILL_AREA_STYLE ('',( #109678 ) ) ;
#212568=PRESENTATION_STYLE_ASSIGNMENT (( #52216 ) ) ;
#212736=EDGE_CURVE ( 'NONE', #157195, #74610, #58352, .T. ) ;
#212843=DIRECTION ( 'NONE',  ( 3.122502256758252154E-17, 2.602085213965210950E-17, 1.000000000000000000 ) ) ;
#213429=ORIENTED_EDGE ( 'NONE', *, *, #76187, .T. ) ;
#213440=( LENGTH_UNIT ( ) NAMED_UNIT ( * ) SI_UNIT ( .MILLI., .METRE. ) );
#213750=ADVANCED_FACE ( 'NONE', ( #48847 ), #141582, .T. ) ;
ENDSEC;
END-ISO-10303-21;
